ISO-10303-21;
HEADER;
/* Generated by software containing ST-Developer
 * from STEP Tools, Inc. (www.steptools.com) 
 */

FILE_DESCRIPTION(
/* description */ ('Lever-operated bar clamp (toggle)'),
/* implementation_level */ '2;1');

FILE_NAME(
/* name */ 'Socket Set Screw - M4x6.step',
/* time_stamp */ '2026-10-28T03:25:02-07:00',
/* author */ (''),
/* organization */ (''),
/* preprocessor_version */ 'ST-DEVELOPER v20.2',
/* originating_system */ 'Autodesk Translation Framework v15.17.0.0',
/* authorisation */ '');

FILE_SCHEMA (('AUTOMOTIVE_DESIGN { 1 0 10303 214 3 1 1 }'));
ENDSEC;

DATA;
#10=MECHANICAL_DESIGN_GEOMETRIC_PRESENTATION_REPRESENTATION('',(#456),#12413);
#324=CONICAL_SURFACE('',#7879,0.185,0.785398163397449);
#325=CONICAL_SURFACE('',#7883,0.1625,0.785398163397449);
#371=SHAPE_REPRESENTATION_RELATIONSHIP('SRR','None',#12615,#409);
#409=ADVANCED_BREP_SHAPE_REPRESENTATION('',(#499),#12412);
#456=STYLED_ITEM('',(#12876),#499);
#499=MANIFOLD_SOLID_BREP('Body1',#6619);
#650=FACE_BOUND('',#1846,.T.);
#879=PLANE('',#7870);
#880=PLANE('',#7871);
#881=PLANE('',#7872);
#882=PLANE('',#7873);
#883=PLANE('',#7874);
#884=PLANE('',#7875);
#885=PLANE('',#7876);
#886=PLANE('',#7877);
#887=PLANE('',#7885);
#1282=FACE_OUTER_BOUND('',#1838,.T.);
#1283=FACE_OUTER_BOUND('',#1839,.T.);
#1284=FACE_OUTER_BOUND('',#1840,.T.);
#1285=FACE_OUTER_BOUND('',#1841,.T.);
#1286=FACE_OUTER_BOUND('',#1842,.T.);
#1287=FACE_OUTER_BOUND('',#1843,.T.);
#1288=FACE_OUTER_BOUND('',#1844,.T.);
#1289=FACE_OUTER_BOUND('',#1845,.T.);
#1290=FACE_OUTER_BOUND('',#1847,.T.);
#1291=FACE_OUTER_BOUND('',#1848,.T.);
#1292=FACE_OUTER_BOUND('',#1849,.T.);
#1293=FACE_OUTER_BOUND('',#1850,.T.);
#1838=EDGE_LOOP('',(#5983,#5984,#5985,#5986));
#1839=EDGE_LOOP('',(#5987,#5988,#5989,#5990));
#1840=EDGE_LOOP('',(#5991,#5992,#5993,#5994));
#1841=EDGE_LOOP('',(#5995,#5996,#5997,#5998));
#1842=EDGE_LOOP('',(#5999,#6000,#6001,#6002));
#1843=EDGE_LOOP('',(#6003,#6004,#6005,#6006));
#1844=EDGE_LOOP('',(#6007,#6008,#6009,#6010,#6011,#6012));
#1845=EDGE_LOOP('',(#6013));
#1846=EDGE_LOOP('',(#6014,#6015,#6016,#6017,#6018,#6019));
#1847=EDGE_LOOP('',(#6020,#6021,#6022,#6023));
#1848=EDGE_LOOP('',(#6024,#6025,#6026,#6027));
#1849=EDGE_LOOP('',(#6028,#6029,#6030,#6031));
#1850=EDGE_LOOP('',(#6032));
#2271=LINE('',#12264,#2712);
#2272=LINE('',#12266,#2713);
#2273=LINE('',#12268,#2714);
#2274=LINE('',#12269,#2715);
#2275=LINE('',#12272,#2716);
#2276=LINE('',#12274,#2717);
#2277=LINE('',#12275,#2718);
#2278=LINE('',#12278,#2719);
#2279=LINE('',#12280,#2720);
#2280=LINE('',#12281,#2721);
#2281=LINE('',#12284,#2722);
#2282=LINE('',#12286,#2723);
#2283=LINE('',#12287,#2724);
#2284=LINE('',#12290,#2725);
#2285=LINE('',#12292,#2726);
#2286=LINE('',#12293,#2727);
#2287=LINE('',#12295,#2728);
#2288=LINE('',#12296,#2729);
#2289=LINE('',#12304,#2730);
#2290=LINE('',#12308,#2731);
#2291=LINE('',#12312,#2732);
#2712=VECTOR('',#9978,1.);
#2713=VECTOR('',#9979,1.);
#2714=VECTOR('',#9980,1.);
#2715=VECTOR('',#9981,1.);
#2716=VECTOR('',#9984,1.);
#2717=VECTOR('',#9985,1.);
#2718=VECTOR('',#9986,1.);
#2719=VECTOR('',#9989,1.);
#2720=VECTOR('',#9990,1.);
#2721=VECTOR('',#9991,1.);
#2722=VECTOR('',#9994,1.);
#2723=VECTOR('',#9995,1.);
#2724=VECTOR('',#9996,1.);
#2725=VECTOR('',#9999,1.);
#2726=VECTOR('',#10000,1.);
#2727=VECTOR('',#10001,1.);
#2728=VECTOR('',#10004,1.);
#2729=VECTOR('',#10005,1.);
#2730=VECTOR('',#10016,0.185);
#2731=VECTOR('',#10021,0.2);
#2732=VECTOR('',#10026,0.1625);
#3070=CIRCLE('',#7878,0.17);
#3071=CIRCLE('',#7880,0.1954);
#3072=CIRCLE('',#7882,0.1954);
#3073=CIRCLE('',#7884,0.125);
#3599=VERTEX_POINT('',#12262);
#3600=VERTEX_POINT('',#12263);
#3601=VERTEX_POINT('',#12265);
#3602=VERTEX_POINT('',#12267);
#3603=VERTEX_POINT('',#12271);
#3604=VERTEX_POINT('',#12273);
#3605=VERTEX_POINT('',#12277);
#3606=VERTEX_POINT('',#12279);
#3607=VERTEX_POINT('',#12283);
#3608=VERTEX_POINT('',#12285);
#3609=VERTEX_POINT('',#12289);
#3610=VERTEX_POINT('',#12291);
#3611=VERTEX_POINT('',#12299);
#3612=VERTEX_POINT('',#12302);
#3613=VERTEX_POINT('',#12306);
#3614=VERTEX_POINT('',#12310);
#4396=EDGE_CURVE('',#3599,#3600,#2271,.T.);
#4397=EDGE_CURVE('',#3599,#3601,#2272,.T.);
#4398=EDGE_CURVE('',#3601,#3602,#2273,.T.);
#4399=EDGE_CURVE('',#3600,#3602,#2274,.T.);
#4400=EDGE_CURVE('',#3603,#3599,#2275,.T.);
#4401=EDGE_CURVE('',#3603,#3604,#2276,.T.);
#4402=EDGE_CURVE('',#3604,#3601,#2277,.T.);
#4403=EDGE_CURVE('',#3605,#3603,#2278,.T.);
#4404=EDGE_CURVE('',#3605,#3606,#2279,.T.);
#4405=EDGE_CURVE('',#3606,#3604,#2280,.T.);
#4406=EDGE_CURVE('',#3607,#3605,#2281,.T.);
#4407=EDGE_CURVE('',#3607,#3608,#2282,.T.);
#4408=EDGE_CURVE('',#3608,#3606,#2283,.T.);
#4409=EDGE_CURVE('',#3609,#3607,#2284,.T.);
#4410=EDGE_CURVE('',#3609,#3610,#2285,.T.);
#4411=EDGE_CURVE('',#3610,#3608,#2286,.T.);
#4412=EDGE_CURVE('',#3600,#3609,#2287,.T.);
#4413=EDGE_CURVE('',#3602,#3610,#2288,.T.);
#4414=EDGE_CURVE('',#3611,#3611,#3070,.T.);
#4415=EDGE_CURVE('',#3612,#3612,#3071,.T.);
#4416=EDGE_CURVE('',#3612,#3611,#2289,.T.);
#4417=EDGE_CURVE('',#3613,#3613,#3072,.F.);
#4418=EDGE_CURVE('',#3613,#3612,#2290,.T.);
#4419=EDGE_CURVE('',#3614,#3614,#3073,.T.);
#4420=EDGE_CURVE('',#3614,#3613,#2291,.T.);
#5983=ORIENTED_EDGE('',*,*,#4396,.F.);
#5984=ORIENTED_EDGE('',*,*,#4397,.T.);
#5985=ORIENTED_EDGE('',*,*,#4398,.T.);
#5986=ORIENTED_EDGE('',*,*,#4399,.F.);
#5987=ORIENTED_EDGE('',*,*,#4400,.F.);
#5988=ORIENTED_EDGE('',*,*,#4401,.T.);
#5989=ORIENTED_EDGE('',*,*,#4402,.T.);
#5990=ORIENTED_EDGE('',*,*,#4397,.F.);
#5991=ORIENTED_EDGE('',*,*,#4403,.F.);
#5992=ORIENTED_EDGE('',*,*,#4404,.T.);
#5993=ORIENTED_EDGE('',*,*,#4405,.T.);
#5994=ORIENTED_EDGE('',*,*,#4401,.F.);
#5995=ORIENTED_EDGE('',*,*,#4406,.F.);
#5996=ORIENTED_EDGE('',*,*,#4407,.T.);
#5997=ORIENTED_EDGE('',*,*,#4408,.T.);
#5998=ORIENTED_EDGE('',*,*,#4404,.F.);
#5999=ORIENTED_EDGE('',*,*,#4409,.F.);
#6000=ORIENTED_EDGE('',*,*,#4410,.T.);
#6001=ORIENTED_EDGE('',*,*,#4411,.T.);
#6002=ORIENTED_EDGE('',*,*,#4407,.F.);
#6003=ORIENTED_EDGE('',*,*,#4412,.F.);
#6004=ORIENTED_EDGE('',*,*,#4399,.T.);
#6005=ORIENTED_EDGE('',*,*,#4413,.T.);
#6006=ORIENTED_EDGE('',*,*,#4410,.F.);
#6007=ORIENTED_EDGE('',*,*,#4413,.F.);
#6008=ORIENTED_EDGE('',*,*,#4398,.F.);
#6009=ORIENTED_EDGE('',*,*,#4402,.F.);
#6010=ORIENTED_EDGE('',*,*,#4405,.F.);
#6011=ORIENTED_EDGE('',*,*,#4408,.F.);
#6012=ORIENTED_EDGE('',*,*,#4411,.F.);
#6013=ORIENTED_EDGE('',*,*,#4414,.F.);
#6014=ORIENTED_EDGE('',*,*,#4396,.T.);
#6015=ORIENTED_EDGE('',*,*,#4412,.T.);
#6016=ORIENTED_EDGE('',*,*,#4409,.T.);
#6017=ORIENTED_EDGE('',*,*,#4406,.T.);
#6018=ORIENTED_EDGE('',*,*,#4403,.T.);
#6019=ORIENTED_EDGE('',*,*,#4400,.T.);
#6020=ORIENTED_EDGE('',*,*,#4415,.F.);
#6021=ORIENTED_EDGE('',*,*,#4416,.T.);
#6022=ORIENTED_EDGE('',*,*,#4414,.T.);
#6023=ORIENTED_EDGE('',*,*,#4416,.F.);
#6024=ORIENTED_EDGE('',*,*,#4417,.F.);
#6025=ORIENTED_EDGE('',*,*,#4418,.T.);
#6026=ORIENTED_EDGE('',*,*,#4415,.T.);
#6027=ORIENTED_EDGE('',*,*,#4418,.F.);
#6028=ORIENTED_EDGE('',*,*,#4419,.F.);
#6029=ORIENTED_EDGE('',*,*,#4420,.T.);
#6030=ORIENTED_EDGE('',*,*,#4417,.T.);
#6031=ORIENTED_EDGE('',*,*,#4420,.F.);
#6032=ORIENTED_EDGE('',*,*,#4419,.T.);
#6162=CYLINDRICAL_SURFACE('',#7881,0.1954);
#6557=ADVANCED_FACE('',(#1282),#879,.F.);
#6558=ADVANCED_FACE('',(#1283),#880,.F.);
#6559=ADVANCED_FACE('',(#1284),#881,.F.);
#6560=ADVANCED_FACE('',(#1285),#882,.F.);
#6561=ADVANCED_FACE('',(#1286),#883,.F.);
#6562=ADVANCED_FACE('',(#1287),#884,.F.);
#6563=ADVANCED_FACE('',(#1288),#885,.F.);
#6564=ADVANCED_FACE('',(#1289,#650),#886,.T.);
#6565=ADVANCED_FACE('',(#1290),#324,.T.);
#6566=ADVANCED_FACE('',(#1291),#6162,.T.);
#6567=ADVANCED_FACE('',(#1292),#325,.T.);
#6568=ADVANCED_FACE('',(#1293),#887,.T.);
#6619=CLOSED_SHELL('',(#6557,#6558,#6559,#6560,#6561,#6562,#6563,#6564,
#6565,#6566,#6567,#6568));
#7869=AXIS2_PLACEMENT_3D('',#12260,#9974,#9975);
#7870=AXIS2_PLACEMENT_3D('',#12261,#9976,#9977);
#7871=AXIS2_PLACEMENT_3D('',#12270,#9982,#9983);
#7872=AXIS2_PLACEMENT_3D('',#12276,#9987,#9988);
#7873=AXIS2_PLACEMENT_3D('',#12282,#9992,#9993);
#7874=AXIS2_PLACEMENT_3D('',#12288,#9997,#9998);
#7875=AXIS2_PLACEMENT_3D('',#12294,#10002,#10003);
#7876=AXIS2_PLACEMENT_3D('',#12297,#10006,#10007);
#7877=AXIS2_PLACEMENT_3D('',#12298,#10008,#10009);
#7878=AXIS2_PLACEMENT_3D('',#12300,#10010,#10011);
#7879=AXIS2_PLACEMENT_3D('',#12301,#10012,#10013);
#7880=AXIS2_PLACEMENT_3D('',#12303,#10014,#10015);
#7881=AXIS2_PLACEMENT_3D('',#12305,#10017,#10018);
#7882=AXIS2_PLACEMENT_3D('',#12307,#10019,#10020);
#7883=AXIS2_PLACEMENT_3D('',#12309,#10022,#10023);
#7884=AXIS2_PLACEMENT_3D('',#12311,#10024,#10025);
#7885=AXIS2_PLACEMENT_3D('',#12313,#10027,#10028);
#9974=DIRECTION('axis',(0.,0.,1.));
#9975=DIRECTION('refdir',(1.,0.,0.));
#9976=DIRECTION('center_axis',(0.866025403784439,0.,-0.5));
#9977=DIRECTION('ref_axis',(0.5,0.,0.866025403784439));
#9978=DIRECTION('',(0.5,0.,0.866025403784439));
#9979=DIRECTION('',(0.,-1.,0.));
#9980=DIRECTION('',(0.5,0.,0.866025403784439));
#9981=DIRECTION('',(0.,-1.,0.));
#9982=DIRECTION('center_axis',(1.20185167898973E-16,0.,-1.));
#9983=DIRECTION('ref_axis',(1.,0.,1.20185167898973E-16));
#9984=DIRECTION('',(1.,0.,1.20185167898973E-16));
#9985=DIRECTION('',(0.,-1.,0.));
#9986=DIRECTION('',(1.,0.,1.20185167898973E-16));
#9987=DIRECTION('center_axis',(-0.866025403784439,0.,-0.5));
#9988=DIRECTION('ref_axis',(0.5,0.,-0.866025403784439));
#9989=DIRECTION('',(0.5,0.,-0.866025403784439));
#9990=DIRECTION('',(0.,-1.,0.));
#9991=DIRECTION('',(0.5,0.,-0.866025403784439));
#9992=DIRECTION('center_axis',(-0.866025403784439,0.,0.5));
#9993=DIRECTION('ref_axis',(-0.5,0.,-0.866025403784439));
#9994=DIRECTION('',(-0.5,0.,-0.866025403784439));
#9995=DIRECTION('',(0.,-1.,0.));
#9996=DIRECTION('',(-0.5,0.,-0.866025403784439));
#9997=DIRECTION('center_axis',(-2.40370335797945E-16,0.,1.));
#9998=DIRECTION('ref_axis',(-1.,0.,-2.40370335797945E-16));
#9999=DIRECTION('',(-1.,0.,-2.40370335797945E-16));
#10000=DIRECTION('',(0.,-1.,0.));
#10001=DIRECTION('',(-1.,0.,-2.40370335797945E-16));
#10002=DIRECTION('center_axis',(0.866025403784439,0.,0.5));
#10003=DIRECTION('ref_axis',(-0.5,0.,0.866025403784439));
#10004=DIRECTION('',(-0.5,0.,0.866025403784439));
#10005=DIRECTION('',(-0.5,0.,0.866025403784439));
#10006=DIRECTION('center_axis',(0.,-1.,0.));
#10007=DIRECTION('ref_axis',(0.,0.,-1.));
#10008=DIRECTION('center_axis',(0.,1.,0.));
#10009=DIRECTION('ref_axis',(0.,0.,1.));
#10010=DIRECTION('center_axis',(0.,-1.,0.));
#10011=DIRECTION('ref_axis',(1.,0.,0.));
#10012=DIRECTION('center_axis',(0.,-1.,0.));
#10013=DIRECTION('ref_axis',(1.,0.,0.));
#10014=DIRECTION('center_axis',(0.,-1.,0.));
#10015=DIRECTION('ref_axis',(1.,0.,0.));
#10016=DIRECTION('',(0.707106781186548,0.707106781186547,8.65956056235494E-17));
#10017=DIRECTION('center_axis',(0.,-1.,0.));
#10018=DIRECTION('ref_axis',(1.,0.,0.));
#10019=DIRECTION('center_axis',(0.,1.,0.));
#10020=DIRECTION('ref_axis',(1.,0.,0.));
#10021=DIRECTION('',(0.,1.,0.));
#10022=DIRECTION('center_axis',(0.,1.,0.));
#10023=DIRECTION('ref_axis',(1.,0.,0.));
#10024=DIRECTION('center_axis',(0.,-1.,0.));
#10025=DIRECTION('ref_axis',(1.,0.,0.));
#10026=DIRECTION('',(-0.707106781186548,0.707106781186547,-8.65956056235494E-17));
#10027=DIRECTION('center_axis',(0.,-1.,0.));
#10028=DIRECTION('ref_axis',(0.,0.,-1.));
#12260=CARTESIAN_POINT('',(0.,0.,0.));
#12261=CARTESIAN_POINT('Origin',(0.0577350269189626,0.,-0.1));
#12262=CARTESIAN_POINT('',(0.0577350269189626,0.,-0.1));
#12263=CARTESIAN_POINT('',(0.115470053837925,0.,0.));
#12264=CARTESIAN_POINT('',(0.0934187836487032,0.,-0.0381939203391614));
#12265=CARTESIAN_POINT('',(0.0577350269189626,-0.2,-0.1));
#12266=CARTESIAN_POINT('',(0.0577350269189626,0.,-0.1));
#12267=CARTESIAN_POINT('',(0.115470053837925,-0.2,0.));
#12268=CARTESIAN_POINT('',(0.115470053837925,-0.2,0.));
#12269=CARTESIAN_POINT('',(0.115470053837925,0.,0.));
#12270=CARTESIAN_POINT('Origin',(-0.0577350269189626,0.,-0.1));
#12271=CARTESIAN_POINT('',(-0.0577350269189626,0.,-0.1));
#12272=CARTESIAN_POINT('',(0.0561324865405187,0.,-0.1));
#12273=CARTESIAN_POINT('',(-0.0577350269189626,-0.2,-0.1));
#12274=CARTESIAN_POINT('',(-0.0577350269189626,0.,-0.1));
#12275=CARTESIAN_POINT('',(0.0577350269189626,-0.2,-0.1));
#12276=CARTESIAN_POINT('Origin',(-0.115470053837925,0.,-1.38777878078145E-17));
#12277=CARTESIAN_POINT('',(-0.115470053837925,0.,-1.41410031829988E-17));
#12278=CARTESIAN_POINT('',(-0.0797862971081845,0.,-0.0618060796608387));
#12279=CARTESIAN_POINT('',(-0.115470053837925,-0.2,-1.38777878078145E-17));
#12280=CARTESIAN_POINT('',(-0.115470053837925,0.,-1.41410031829988E-17));
#12281=CARTESIAN_POINT('',(-0.0577350269189626,-0.2,-0.1));
#12282=CARTESIAN_POINT('Origin',(-0.0577350269189626,0.,0.1));
#12283=CARTESIAN_POINT('',(-0.0577350269189626,0.,0.1));
#12284=CARTESIAN_POINT('',(-0.0509187836487033,0.,0.111806079660839));
#12285=CARTESIAN_POINT('',(-0.0577350269189626,-0.2,0.1));
#12286=CARTESIAN_POINT('',(-0.0577350269189626,0.,0.1));
#12287=CARTESIAN_POINT('',(-0.115470053837925,-0.2,-1.41410031829988E-17));
#12288=CARTESIAN_POINT('Origin',(0.0577350269189626,0.,0.1));
#12289=CARTESIAN_POINT('',(0.0577350269189626,0.,0.1));
#12290=CARTESIAN_POINT('',(0.113867513459481,0.,0.1));
#12291=CARTESIAN_POINT('',(0.0577350269189626,-0.2,0.1));
#12292=CARTESIAN_POINT('',(0.0577350269189626,0.,0.1));
#12293=CARTESIAN_POINT('',(-0.0577350269189626,-0.2,0.1));
#12294=CARTESIAN_POINT('Origin',(0.115470053837925,0.,0.));
#12295=CARTESIAN_POINT('',(0.122286297108185,0.,-0.0118060796608386));
#12296=CARTESIAN_POINT('',(0.0577350269189626,-0.2,0.1));
#12297=CARTESIAN_POINT('Origin',(0.,-0.2,0.));
#12298=CARTESIAN_POINT('Origin',(0.17,0.,0.));
#12299=CARTESIAN_POINT('',(-0.17,-8.67361737988404E-18,-2.0818995585505E-17));
#12300=CARTESIAN_POINT('Origin',(0.,0.,0.));
#12301=CARTESIAN_POINT('Origin',(0.,-0.015,0.));
#12302=CARTESIAN_POINT('',(-0.1954,-0.0254,-2.39295984553393E-17));
#12303=CARTESIAN_POINT('Origin',(0.,-0.0254,0.));
#12304=CARTESIAN_POINT('',(-0.185,-0.015,-2.2655965784226E-17));
#12305=CARTESIAN_POINT('Origin',(0.,-0.2775,0.));
#12306=CARTESIAN_POINT('',(-0.1954,-0.5296,2.39295984553393E-17));
#12307=CARTESIAN_POINT('Origin',(0.,-0.5296,0.));
#12308=CARTESIAN_POINT('',(-0.1954,-0.2775,-2.39295984553393E-17));
#12309=CARTESIAN_POINT('Origin',(0.,-0.5625,0.));
#12310=CARTESIAN_POINT('',(-0.125,-0.6,-1.53080849893419E-17));
#12311=CARTESIAN_POINT('Origin',(0.,-0.6,0.));
#12312=CARTESIAN_POINT('',(-0.1625,-0.5625,-1.99005104861445E-17));
#12313=CARTESIAN_POINT('Origin',(0.,-0.6,0.));
#12366=UNCERTAINTY_MEASURE_WITH_UNIT(LENGTH_MEASURE(0.001),#12414,
'DISTANCE_ACCURACY_VALUE',
'Maximum model space distance between geometric entities at asserted c
onnectivities');
#12367=UNCERTAINTY_MEASURE_WITH_UNIT(LENGTH_MEASURE(0.001),#12414,
'DISTANCE_ACCURACY_VALUE',
'Maximum model space distance between geometric entities at asserted c
onnectivities');
#12412=(
GEOMETRIC_REPRESENTATION_CONTEXT(3)
GLOBAL_UNCERTAINTY_ASSIGNED_CONTEXT((#12366))
GLOBAL_UNIT_ASSIGNED_CONTEXT((#12414,#12416,#12417))
REPRESENTATION_CONTEXT('','3D')
);
#12413=(
GEOMETRIC_REPRESENTATION_CONTEXT(3)
GLOBAL_UNCERTAINTY_ASSIGNED_CONTEXT((#12367))
GLOBAL_UNIT_ASSIGNED_CONTEXT((#12414,#12416,#12417))
REPRESENTATION_CONTEXT('','3D')
);
#12414=(
LENGTH_UNIT()
NAMED_UNIT(*)
SI_UNIT(.CENTI.,.METRE.)
);
#12416=(
NAMED_UNIT(*)
PLANE_ANGLE_UNIT()
SI_UNIT($,.RADIAN.)
);
#12417=(
NAMED_UNIT(*)
SI_UNIT($,.STERADIAN.)
SOLID_ANGLE_UNIT()
);
#12462=SHAPE_DEFINITION_REPRESENTATION(#12562,#12615);
#12562=PRODUCT_DEFINITION_SHAPE('',$,#12661);
#12615=SHAPE_REPRESENTATION('',(#7869),#12412);
#12616=PRODUCT_DEFINITION_CONTEXT('part definition',#12753,'design');
#12661=PRODUCT_DEFINITION('Socket Set Screw - M4x6',
'Socket Set Screw - M4x6',#12706,#12616);
#12706=PRODUCT_DEFINITION_FORMATION('',$,#12799);
#12753=APPLICATION_CONTEXT(
'Core Data for Automotive Mechanical Design Process');
#12754=PRODUCT_CONTEXT('part definition',#12753,'mechanical');
#12799=PRODUCT('Socket Set Screw - M4x6','Socket Set Screw - M4x6',
'Socket Set Screw - M4x6',(#12754));
#12870=COLOUR_RGB('Black',0.12,0.14,0.17);
#12871=FILL_AREA_STYLE_COLOUR('',#12870);
#12872=FILL_AREA_STYLE('',(#12871));
#12873=SURFACE_STYLE_FILL_AREA(#12872);
#12874=SURFACE_SIDE_STYLE('',(#12873));
#12875=SURFACE_STYLE_USAGE(.BOTH.,#12874);
#12876=PRESENTATION_STYLE_ASSIGNMENT((#12875));
ENDSEC;
END-ISO-10303-21;
